ISO-10303-21;
HEADER;
/* Generated by software containing ST-Developer
 * from STEP Tools, Inc. (www.steptools.com) 
 */

FILE_DESCRIPTION(
/* description */ ('Torque wrench calibration arm'),
/* implementation_level */ '2;1');

FILE_NAME(
/* name */ 'Balls (1).step',
/* time_stamp */ '2026-10-28T03:24:52-07:00',
/* author */ (''),
/* organization */ (''),
/* preprocessor_version */ 'ST-DEVELOPER v20.2',
/* originating_system */ 'Autodesk Translation Framework v15.17.0.0',
/* authorisation */ '');

FILE_SCHEMA (('AUTOMOTIVE_DESIGN { 1 0 10303 214 3 1 1 }'));
ENDSEC;

DATA;
#10=MECHANICAL_DESIGN_GEOMETRIC_PRESENTATION_REPRESENTATION('',(#460,#461,#462,#463,#464,#465,#466,#467),#12783);
#311=SPHERICAL_SURFACE('',#7579,0.23815);
#312=SPHERICAL_SURFACE('',#7581,0.23815);
#313=SPHERICAL_SURFACE('',#7583,0.23815);
#314=SPHERICAL_SURFACE('',#7585,0.23815);
#315=SPHERICAL_SURFACE('',#7587,0.23815);
#316=SPHERICAL_SURFACE('',#7589,0.23815);
#317=SPHERICAL_SURFACE('',#7591,0.23815);
#318=SPHERICAL_SURFACE('',#7593,0.23815);
#377=SHAPE_REPRESENTATION_RELATIONSHIP('SRR','None',#12961,#414);
#414=ADVANCED_BREP_SHAPE_REPRESENTATION('',(#512,#513,#514,#515,#516,#517,
#518,#519),#12770);
#460=STYLED_ITEM('',(#13212),#512);
#461=STYLED_ITEM('',(#13212),#513);
#462=STYLED_ITEM('',(#13212),#514);
#463=STYLED_ITEM('',(#13212),#515);
#464=STYLED_ITEM('',(#13212),#516);
#465=STYLED_ITEM('',(#13212),#517);
#466=STYLED_ITEM('',(#13212),#518);
#467=STYLED_ITEM('',(#13212),#519);
#512=MANIFOLD_SOLID_BREP('Body1',#6531);
#513=MANIFOLD_SOLID_BREP('Body2',#6532);
#514=MANIFOLD_SOLID_BREP('Body3',#6533);
#515=MANIFOLD_SOLID_BREP('Body4',#6534);
#516=MANIFOLD_SOLID_BREP('Body5',#6535);
#517=MANIFOLD_SOLID_BREP('Body6',#6536);
#518=MANIFOLD_SOLID_BREP('Body7',#6537);
#519=MANIFOLD_SOLID_BREP('Body8',#6538);
#1175=FACE_OUTER_BOUND('',#1665,.T.);
#1176=FACE_OUTER_BOUND('',#1666,.T.);
#1177=FACE_OUTER_BOUND('',#1667,.T.);
#1178=FACE_OUTER_BOUND('',#1668,.T.);
#1179=FACE_OUTER_BOUND('',#1669,.T.);
#1180=FACE_OUTER_BOUND('',#1670,.T.);
#1181=FACE_OUTER_BOUND('',#1671,.T.);
#1182=FACE_OUTER_BOUND('',#1672,.T.);
#1665=EDGE_LOOP('',(#5623,#5624));
#1666=EDGE_LOOP('',(#5625,#5626));
#1667=EDGE_LOOP('',(#5627,#5628));
#1668=EDGE_LOOP('',(#5629,#5630));
#1669=EDGE_LOOP('',(#5631,#5632));
#1670=EDGE_LOOP('',(#5633,#5634));
#1671=EDGE_LOOP('',(#5635,#5636));
#1672=EDGE_LOOP('',(#5637,#5638));
#2878=CIRCLE('',#7580,0.23815);
#2879=CIRCLE('',#7582,0.23815);
#2880=CIRCLE('',#7584,0.23815);
#2881=CIRCLE('',#7586,0.23815);
#2882=CIRCLE('',#7588,0.23815);
#2883=CIRCLE('',#7590,0.23815);
#2884=CIRCLE('',#7592,0.23815);
#2885=CIRCLE('',#7594,0.23815);
#3402=VERTEX_POINT('',#11908);
#3403=VERTEX_POINT('',#11909);
#3404=VERTEX_POINT('',#11912);
#3405=VERTEX_POINT('',#11913);
#3406=VERTEX_POINT('',#11916);
#3407=VERTEX_POINT('',#11917);
#3408=VERTEX_POINT('',#11920);
#3409=VERTEX_POINT('',#11921);
#3410=VERTEX_POINT('',#11924);
#3411=VERTEX_POINT('',#11925);
#3412=VERTEX_POINT('',#11928);
#3413=VERTEX_POINT('',#11929);
#3414=VERTEX_POINT('',#11932);
#3415=VERTEX_POINT('',#11933);
#3416=VERTEX_POINT('',#11936);
#3417=VERTEX_POINT('',#11937);
#4169=EDGE_CURVE('',#3402,#3403,#2878,.T.);
#4170=EDGE_CURVE('',#3404,#3405,#2879,.T.);
#4171=EDGE_CURVE('',#3406,#3407,#2880,.T.);
#4172=EDGE_CURVE('',#3408,#3409,#2881,.T.);
#4173=EDGE_CURVE('',#3410,#3411,#2882,.T.);
#4174=EDGE_CURVE('',#3412,#3413,#2883,.T.);
#4175=EDGE_CURVE('',#3414,#3415,#2884,.T.);
#4176=EDGE_CURVE('',#3416,#3417,#2885,.T.);
#5623=ORIENTED_EDGE('',*,*,#4169,.T.);
#5624=ORIENTED_EDGE('',*,*,#4169,.F.);
#5625=ORIENTED_EDGE('',*,*,#4170,.T.);
#5626=ORIENTED_EDGE('',*,*,#4170,.F.);
#5627=ORIENTED_EDGE('',*,*,#4171,.T.);
#5628=ORIENTED_EDGE('',*,*,#4171,.F.);
#5629=ORIENTED_EDGE('',*,*,#4172,.T.);
#5630=ORIENTED_EDGE('',*,*,#4172,.F.);
#5631=ORIENTED_EDGE('',*,*,#4173,.T.);
#5632=ORIENTED_EDGE('',*,*,#4173,.F.);
#5633=ORIENTED_EDGE('',*,*,#4174,.T.);
#5634=ORIENTED_EDGE('',*,*,#4174,.F.);
#5635=ORIENTED_EDGE('',*,*,#4175,.T.);
#5636=ORIENTED_EDGE('',*,*,#4175,.F.);
#5637=ORIENTED_EDGE('',*,*,#4176,.T.);
#5638=ORIENTED_EDGE('',*,*,#4176,.F.);
#6400=ADVANCED_FACE('',(#1175),#311,.T.);
#6401=ADVANCED_FACE('',(#1176),#312,.T.);
#6402=ADVANCED_FACE('',(#1177),#313,.T.);
#6403=ADVANCED_FACE('',(#1178),#314,.T.);
#6404=ADVANCED_FACE('',(#1179),#315,.T.);
#6405=ADVANCED_FACE('',(#1180),#316,.T.);
#6406=ADVANCED_FACE('',(#1181),#317,.T.);
#6407=ADVANCED_FACE('',(#1182),#318,.T.);
#6531=CLOSED_SHELL('',(#6400));
#6532=CLOSED_SHELL('',(#6401));
#6533=CLOSED_SHELL('',(#6402));
#6534=CLOSED_SHELL('',(#6403));
#6535=CLOSED_SHELL('',(#6404));
#6536=CLOSED_SHELL('',(#6405));
#6537=CLOSED_SHELL('',(#6406));
#6538=CLOSED_SHELL('',(#6407));
#7578=AXIS2_PLACEMENT_3D('',#11906,#9390,#9391);
#7579=AXIS2_PLACEMENT_3D('',#11907,#9392,#9393);
#7580=AXIS2_PLACEMENT_3D('',#11910,#9394,#9395);
#7581=AXIS2_PLACEMENT_3D('',#11911,#9396,#9397);
#7582=AXIS2_PLACEMENT_3D('',#11914,#9398,#9399);
#7583=AXIS2_PLACEMENT_3D('',#11915,#9400,#9401);
#7584=AXIS2_PLACEMENT_3D('',#11918,#9402,#9403);
#7585=AXIS2_PLACEMENT_3D('',#11919,#9404,#9405);
#7586=AXIS2_PLACEMENT_3D('',#11922,#9406,#9407);
#7587=AXIS2_PLACEMENT_3D('',#11923,#9408,#9409);
#7588=AXIS2_PLACEMENT_3D('',#11926,#9410,#9411);
#7589=AXIS2_PLACEMENT_3D('',#11927,#9412,#9413);
#7590=AXIS2_PLACEMENT_3D('',#11930,#9414,#9415);
#7591=AXIS2_PLACEMENT_3D('',#11931,#9416,#9417);
#7592=AXIS2_PLACEMENT_3D('',#11934,#9418,#9419);
#7593=AXIS2_PLACEMENT_3D('',#11935,#9420,#9421);
#7594=AXIS2_PLACEMENT_3D('',#11938,#9422,#9423);
#9390=DIRECTION('axis',(0.,0.,1.));
#9391=DIRECTION('refdir',(1.,0.,0.));
#9392=DIRECTION('center_axis',(0.,0.,1.));
#9393=DIRECTION('ref_axis',(1.,0.,0.));
#9394=DIRECTION('center_axis',(1.22464679914735E-16,-1.,0.));
#9395=DIRECTION('ref_axis',(-1.,-1.22464679914735E-16,0.));
#9396=DIRECTION('center_axis',(0.707106781186548,0.,0.707106781186548));
#9397=DIRECTION('ref_axis',(0.707106781186548,0.,-0.707106781186548));
#9398=DIRECTION('center_axis',(8.65956056235494E-17,-1.,-8.65956056235493E-17));
#9399=DIRECTION('ref_axis',(-0.707106781186547,-1.22464679914735E-16,0.707106781186547));
#9400=DIRECTION('center_axis',(1.,0.,0.));
#9401=DIRECTION('ref_axis',(6.12323399573676E-17,0.,-1.));
#9402=DIRECTION('center_axis',(7.49879891330929E-33,-1.,-1.22464679914735E-16));
#9403=DIRECTION('ref_axis',(-6.12323399573676E-17,-1.22464679914735E-16,
1.));
#9404=DIRECTION('center_axis',(0.707106781186548,0.,-0.707106781186548));
#9405=DIRECTION('ref_axis',(-0.707106781186548,0.,-0.707106781186548));
#9406=DIRECTION('center_axis',(-8.65956056235493E-17,-1.,-8.65956056235494E-17));
#9407=DIRECTION('ref_axis',(0.707106781186547,-1.22464679914735E-16,0.707106781186547));
#9408=DIRECTION('center_axis',(0.,0.,-1.));
#9409=DIRECTION('ref_axis',(-1.,0.,-1.22464679914735E-16));
#9410=DIRECTION('center_axis',(-1.22464679914735E-16,-1.,-1.49975978266186E-32));
#9411=DIRECTION('ref_axis',(1.,-1.22464679914735E-16,1.22464679914735E-16));
#9412=DIRECTION('center_axis',(-0.707106781186547,0.,-0.707106781186548));
#9413=DIRECTION('ref_axis',(-0.707106781186548,0.,0.707106781186547));
#9414=DIRECTION('center_axis',(-8.65956056235493E-17,-1.,8.65956056235493E-17));
#9415=DIRECTION('ref_axis',(0.707106781186548,-1.22464679914735E-16,-0.707106781186547));
#9416=DIRECTION('center_axis',(-1.,0.,0.));
#9417=DIRECTION('ref_axis',(-1.83697019872103E-16,0.,1.));
#9418=DIRECTION('center_axis',(-2.24963967399279E-32,-1.,1.22464679914735E-16));
#9419=DIRECTION('ref_axis',(1.83697019872103E-16,-1.22464679914735E-16,
-1.));
#9420=DIRECTION('center_axis',(-0.707106781186548,0.,0.707106781186548));
#9421=DIRECTION('ref_axis',(0.707106781186547,0.,0.707106781186548));
#9422=DIRECTION('center_axis',(8.65956056235493E-17,-1.,8.65956056235493E-17));
#9423=DIRECTION('ref_axis',(-0.707106781186547,-1.22464679914735E-16,-0.707106781186548));
#11906=CARTESIAN_POINT('',(0.,0.,0.));
#11907=CARTESIAN_POINT('Origin',(1.,0.,0.));
#11908=CARTESIAN_POINT('',(1.,-1.78583896120461E-33,0.23815));
#11909=CARTESIAN_POINT('',(1.,-1.78583896120461E-33,-0.23815));
#11910=CARTESIAN_POINT('Origin',(1.,0.,0.));
#11911=CARTESIAN_POINT('Origin',(0.707106781186548,0.,-0.707106781186547));
#11912=CARTESIAN_POINT('',(0.875504261126124,-1.78583896120461E-33,-0.538709301246971));
#11913=CARTESIAN_POINT('',(0.538709301246971,-1.78583896120461E-33,-0.875504261126124));
#11914=CARTESIAN_POINT('Origin',(0.707106781186548,0.,-0.707106781186547));
#11915=CARTESIAN_POINT('Origin',(6.12323399573677E-17,0.,-1.));
#11916=CARTESIAN_POINT('',(0.23815,-1.78583896120461E-33,-1.));
#11917=CARTESIAN_POINT('',(-0.23815,-1.78583896120461E-33,-1.));
#11918=CARTESIAN_POINT('Origin',(6.12323399573677E-17,0.,-1.));
#11919=CARTESIAN_POINT('Origin',(-0.707106781186547,0.,-0.707106781186548));
#11920=CARTESIAN_POINT('',(-0.538709301246971,-1.78583896120461E-33,-0.875504261126124));
#11921=CARTESIAN_POINT('',(-0.875504261126124,-1.78583896120461E-33,-0.538709301246971));
#11922=CARTESIAN_POINT('Origin',(-0.707106781186547,0.,-0.707106781186548));
#11923=CARTESIAN_POINT('Origin',(-1.,0.,-1.22464679914735E-16));
#11924=CARTESIAN_POINT('',(-1.,-1.78583896120461E-33,-0.23815));
#11925=CARTESIAN_POINT('',(-1.,-1.78583896120461E-33,0.23815));
#11926=CARTESIAN_POINT('Origin',(-1.,0.,-1.22464679914735E-16));
#11927=CARTESIAN_POINT('Origin',(-0.707106781186548,0.,0.707106781186547));
#11928=CARTESIAN_POINT('',(-0.875504261126124,-7.94881478324376E-33,0.538709301246971));
#11929=CARTESIAN_POINT('',(-0.538709301246971,4.37713686083455E-33,0.875504261126124));
#11930=CARTESIAN_POINT('Origin',(-0.707106781186548,0.,0.707106781186547));
#11931=CARTESIAN_POINT('Origin',(-1.83697019872103E-16,0.,1.));
#11932=CARTESIAN_POINT('',(-0.23815,-1.78583896120461E-33,1.));
#11933=CARTESIAN_POINT('',(0.23815,-1.78583896120461E-33,1.));
#11934=CARTESIAN_POINT('Origin',(-1.83697019872103E-16,0.,1.));
#11935=CARTESIAN_POINT('Origin',(0.707106781186547,0.,0.707106781186548));
#11936=CARTESIAN_POINT('',(0.538709301246971,-4.86732687222419E-33,0.875504261126124));
#11937=CARTESIAN_POINT('',(0.875504261126124,1.29564894981497E-33,0.538709301246971));
#11938=CARTESIAN_POINT('Origin',(0.707106781186547,0.,0.707106781186548));
#12726=UNCERTAINTY_MEASURE_WITH_UNIT(LENGTH_MEASURE(0.001),#12784,
'DISTANCE_ACCURACY_VALUE',
'Maximum model space distance between geometric entities at asserted c
onnectivities');
#12739=UNCERTAINTY_MEASURE_WITH_UNIT(LENGTH_MEASURE(0.001),#12784,
'DISTANCE_ACCURACY_VALUE',
'Maximum model space distance between geometric entities at asserted c
onnectivities');
#12770=(
GEOMETRIC_REPRESENTATION_CONTEXT(3)
GLOBAL_UNCERTAINTY_ASSIGNED_CONTEXT((#12726))
GLOBAL_UNIT_ASSIGNED_CONTEXT((#12784,#12786,#12787))
REPRESENTATION_CONTEXT('','3D')
);
#12783=(
GEOMETRIC_REPRESENTATION_CONTEXT(3)
GLOBAL_UNCERTAINTY_ASSIGNED_CONTEXT((#12739))
GLOBAL_UNIT_ASSIGNED_CONTEXT((#12784,#12786,#12787))
REPRESENTATION_CONTEXT('','3D')
);
#12784=(
LENGTH_UNIT()
NAMED_UNIT(*)
SI_UNIT(.CENTI.,.METRE.)
);
#12786=(
NAMED_UNIT(*)
PLANE_ANGLE_UNIT()
SI_UNIT($,.RADIAN.)
);
#12787=(
NAMED_UNIT(*)
SI_UNIT($,.STERADIAN.)
SOLID_ANGLE_UNIT()
);
#12818=SHAPE_DEFINITION_REPRESENTATION(#12887,#12961);
#12887=PRODUCT_DEFINITION_SHAPE('',$,#13005);
#12961=SHAPE_REPRESENTATION('',(#7578),#12770);
#12974=PRODUCT_DEFINITION_CONTEXT('part definition',#13105,'design');
#13005=PRODUCT_DEFINITION('Balls (1)','Balls (1)',#13048,#12974);
#13048=PRODUCT_DEFINITION_FORMATION('',$,#13137);
#13105=APPLICATION_CONTEXT(
'Core Data for Automotive Mechanical Design Process');
#13106=PRODUCT_CONTEXT('part definition',#13105,'mechanical');
#13137=PRODUCT('Balls (1)','Balls (1)','Balls (1)',(#13106));
#13206=COLOUR_RGB('Grey',0.48,0.52,0.57);
#13207=FILL_AREA_STYLE_COLOUR('',#13206);
#13208=FILL_AREA_STYLE('',(#13207));
#13209=SURFACE_STYLE_FILL_AREA(#13208);
#13210=SURFACE_SIDE_STYLE('',(#13209));
#13211=SURFACE_STYLE_USAGE(.BOTH.,#13210);
#13212=PRESENTATION_STYLE_ASSIGNMENT((#13211));
ENDSEC;
END-ISO-10303-21;
